ISO-10303-21;
HEADER;
/* Generated by software containing ST-Developer
 * from STEP Tools, Inc. (www.steptools.com) 
 */

FILE_DESCRIPTION(
/* description */ ('STEP AP214'),
/* implementation_level */ '2;1');

FILE_NAME(
/* name */ 'PRT-RH-1004-02.step',
/* time_stamp */ '2026-10-07T12:49:37-07:00',
/* author */ (''),
/* organization */ (''),
/* preprocessor_version */ 'ST-DEVELOPER v20.2',
/* originating_system */ 'Autodesk Translation Framework v15.15.0.0',
/* authorisation */ '');

FILE_SCHEMA (('AUTOMOTIVE_DESIGN { 1 0 10303 214 3 1 1 }'));
ENDSEC;

DATA;
#10=MECHANICAL_DESIGN_GEOMETRIC_PRESENTATION_REPRESENTATION('',(#288),#33016);
#181=(
BOUNDED_CURVE()
B_SPLINE_CURVE(2,(#17665,#17666,#17667),.UNSPECIFIED.,.F.,.F.)
B_SPLINE_CURVE_WITH_KNOTS((3,3),(2.46691230608693,6.35979033590771),
 .UNSPECIFIED.)
CURVE()
GEOMETRIC_REPRESENTATION_ITEM()
RATIONAL_B_SPLINE_CURVE((3.22754685436793,4.30337260646696,3.22754685436793))
REPRESENTATION_ITEM('')
);
#182=(
BOUNDED_CURVE()
B_SPLINE_CURVE(2,(#17675,#17676,#17677),.UNSPECIFIED.,.F.,.F.)
B_SPLINE_CURVE_WITH_KNOTS((3,3),(4.17496097336999,4.50967143376594),
 .UNSPECIFIED.)
CURVE()
GEOMETRIC_REPRESENTATION_ITEM()
RATIONAL_B_SPLINE_CURVE((2.9510230504805,2.95682766860845,2.9510230504805))
REPRESENTATION_ITEM('')
);
#183=(
BOUNDED_CURVE()
B_SPLINE_CURVE(2,(#17683,#17684,#17685),.UNSPECIFIED.,.F.,.F.)
B_SPLINE_CURVE_WITH_KNOTS((3,3),(2.46691230608693,6.35979033590772),
 .UNSPECIFIED.)
CURVE()
GEOMETRIC_REPRESENTATION_ITEM()
RATIONAL_B_SPLINE_CURVE((3.22754685436793,4.30337260646696,3.22754685436793))
REPRESENTATION_ITEM('')
);
#184=(
BOUNDED_CURVE()
B_SPLINE_CURVE(2,(#17691,#17692,#17693),.UNSPECIFIED.,.F.,.F.)
B_SPLINE_CURVE_WITH_KNOTS((3,3),(4.17496097336998,4.50967143376594),
 .UNSPECIFIED.)
CURVE()
GEOMETRIC_REPRESENTATION_ITEM()
RATIONAL_B_SPLINE_CURVE((2.9510230504805,2.95682766860845,2.9510230504805))
REPRESENTATION_ITEM('')
);
#185=(
BOUNDED_CURVE()
B_SPLINE_CURVE(2,(#17699,#17700,#17701),.UNSPECIFIED.,.F.,.F.)
B_SPLINE_CURVE_WITH_KNOTS((3,3),(2.46691230608693,4.41335132099732),
 .UNSPECIFIED.)
CURVE()
GEOMETRIC_REPRESENTATION_ITEM()
RATIONAL_B_SPLINE_CURVE((3.22754685436793,3.76545973041745,3.76545973041745))
REPRESENTATION_ITEM('')
);
#186=(
BOUNDED_CURVE()
B_SPLINE_CURVE(2,(#17706,#17707,#17708),.UNSPECIFIED.,.F.,.F.)
B_SPLINE_CURVE_WITH_KNOTS((3,3),(4.41335132099732,6.35979033590771),
 .UNSPECIFIED.)
CURVE()
GEOMETRIC_REPRESENTATION_ITEM()
RATIONAL_B_SPLINE_CURVE((3.76545973041745,3.76545973041745,3.22754685436793))
REPRESENTATION_ITEM('')
);
#187=(
BOUNDED_CURVE()
B_SPLINE_CURVE(2,(#17711,#17712,#17713),.UNSPECIFIED.,.F.,.F.)
B_SPLINE_CURVE_WITH_KNOTS((3,3),(4.17496097337,4.50967143376595),
 .UNSPECIFIED.)
CURVE()
GEOMETRIC_REPRESENTATION_ITEM()
RATIONAL_B_SPLINE_CURVE((2.9510230504805,2.95682766860845,2.9510230504805))
REPRESENTATION_ITEM('')
);
#188=(
BOUNDED_CURVE()
B_SPLINE_CURVE(2,(#17719,#17720,#17721),.UNSPECIFIED.,.F.,.F.)
B_SPLINE_CURVE_WITH_KNOTS((3,3),(2.46691230608693,6.35979033590771),
 .UNSPECIFIED.)
CURVE()
GEOMETRIC_REPRESENTATION_ITEM()
RATIONAL_B_SPLINE_CURVE((3.22754685436793,4.30337260646696,3.22754685436793))
REPRESENTATION_ITEM('')
);
#189=(
BOUNDED_CURVE()
B_SPLINE_CURVE(2,(#17728,#17729,#17730),.UNSPECIFIED.,.F.,.F.)
B_SPLINE_CURVE_WITH_KNOTS((3,3),(4.17496097336999,4.50967143376593),
 .UNSPECIFIED.)
CURVE()
GEOMETRIC_REPRESENTATION_ITEM()
RATIONAL_B_SPLINE_CURVE((2.9510230504805,2.95682766860845,2.9510230504805))
REPRESENTATION_ITEM('')
);
#234=SHAPE_REPRESENTATION_RELATIONSHIP('SRR','None',#33127,#261);
#261=ADVANCED_BREP_SHAPE_REPRESENTATION('',(#319),#32988);
#288=STYLED_ITEM('',(#33284),#319);
#319=MANIFOLD_SOLID_BREP('Body1',#9943);
#346=CONICAL_SURFACE('',#10575,6.08697438789325,1.13446401379632);
#347=CONICAL_SURFACE('',#10578,19.5,0.785398163397434);
#348=CONICAL_SURFACE('',#10579,5.,0.785398163397453);
#481=FACE_BOUND('',#1744,.T.);
#482=FACE_BOUND('',#1748,.T.);
#483=FACE_BOUND('',#1751,.T.);
#484=FACE_BOUND('',#1754,.T.);
#485=FACE_BOUND('',#1755,.T.);
#486=FACE_BOUND('',#1757,.T.);
#487=FACE_BOUND('',#1760,.T.);
#488=FACE_BOUND('',#1762,.T.);
#489=FACE_BOUND('',#1768,.T.);
#490=FACE_BOUND('',#1772,.T.);
#843=PLANE('',#10520);
#844=PLANE('',#10521);
#845=PLANE('',#10522);
#846=PLANE('',#10523);
#847=PLANE('',#10524);
#848=PLANE('',#10525);
#849=PLANE('',#10526);
#850=PLANE('',#10528);
#851=PLANE('',#10534);
#852=PLANE('',#10540);
#853=PLANE('',#10544);
#854=PLANE('',#10547);
#855=PLANE('',#10552);
#856=PLANE('',#10553);
#857=PLANE('',#10563);
#858=PLANE('',#10564);
#859=PLANE('',#10566);
#860=PLANE('',#10567);
#861=PLANE('',#10568);
#862=PLANE('',#10569);
#863=PLANE('',#10574);
#864=PLANE('',#10577);
#1174=FACE_OUTER_BOUND('',#1737,.T.);
#1175=FACE_OUTER_BOUND('',#1738,.T.);
#1176=FACE_OUTER_BOUND('',#1739,.T.);
#1177=FACE_OUTER_BOUND('',#1740,.T.);
#1178=FACE_OUTER_BOUND('',#1741,.T.);
#1179=FACE_OUTER_BOUND('',#1742,.T.);
#1180=FACE_OUTER_BOUND('',#1743,.T.);
#1181=FACE_OUTER_BOUND('',#1745,.T.);
#1182=FACE_OUTER_BOUND('',#1746,.T.);
#1183=FACE_OUTER_BOUND('',#1747,.T.);
#1184=FACE_OUTER_BOUND('',#1749,.T.);
#1185=FACE_OUTER_BOUND('',#1750,.T.);
#1186=FACE_OUTER_BOUND('',#1752,.T.);
#1187=FACE_OUTER_BOUND('',#1753,.T.);
#1188=FACE_OUTER_BOUND('',#1756,.T.);
#1189=FACE_OUTER_BOUND('',#1758,.T.);
#1190=FACE_OUTER_BOUND('',#1759,.T.);
#1191=FACE_OUTER_BOUND('',#1761,.T.);
#1192=FACE_OUTER_BOUND('',#1763,.T.);
#1193=FACE_OUTER_BOUND('',#1764,.T.);
#1194=FACE_OUTER_BOUND('',#1765,.T.);
#1195=FACE_OUTER_BOUND('',#1766,.T.);
#1196=FACE_OUTER_BOUND('',#1767,.T.);
#1197=FACE_OUTER_BOUND('',#1769,.T.);
#1198=FACE_OUTER_BOUND('',#1770,.T.);
#1199=FACE_OUTER_BOUND('',#1771,.T.);
#1200=FACE_OUTER_BOUND('',#1773,.T.);
#1201=FACE_OUTER_BOUND('',#1774,.T.);
#1202=FACE_OUTER_BOUND('',#1775,.T.);
#1203=FACE_OUTER_BOUND('',#1776,.T.);
#1204=FACE_OUTER_BOUND('',#1777,.T.);
#1205=FACE_OUTER_BOUND('',#1778,.T.);
#1206=FACE_OUTER_BOUND('',#1779,.T.);
#1207=FACE_OUTER_BOUND('',#1780,.T.);
#1737=EDGE_LOOP('',(#7288,#7289,#7290,#7291));
#1738=EDGE_LOOP('',(#7292,#7293,#7294,#7295));
#1739=EDGE_LOOP('',(#7296,#7297,#7298,#7299));
#1740=EDGE_LOOP('',(#7300,#7301,#7302,#7303));
#1741=EDGE_LOOP('',(#7304,#7305,#7306,#7307,#7308));
#1742=EDGE_LOOP('',(#7309,#7310,#7311,#7312));
#1743=EDGE_LOOP('',(#7313,#7314,#7315,#7316));
#1744=EDGE_LOOP('',(#7317));
#1745=EDGE_LOOP('',(#7318,#7319,#7320,#7321));
#1746=EDGE_LOOP('',(#7322,#7323,#7324,#7325,#7326,#7327,#7328,#7329,#7330,
#7331));
#1747=EDGE_LOOP('',(#7332));
#1748=EDGE_LOOP('',(#7333));
#1749=EDGE_LOOP('',(#7334,#7335,#7336,#7337,#7338));
#1750=EDGE_LOOP('',(#7339));
#1751=EDGE_LOOP('',(#7340));
#1752=EDGE_LOOP('',(#7341,#7342,#7343,#7344));
#1753=EDGE_LOOP('',(#7345));
#1754=EDGE_LOOP('',(#7346));
#1755=EDGE_LOOP('',(#7347));
#1756=EDGE_LOOP('',(#7348));
#1757=EDGE_LOOP('',(#7349));
#1758=EDGE_LOOP('',(#7350,#7351,#7352,#7353));
#1759=EDGE_LOOP('',(#7354));
#1760=EDGE_LOOP('',(#7355));
#1761=EDGE_LOOP('',(#7356));
#1762=EDGE_LOOP('',(#7357,#7358,#7359,#7360,#7361,#7362,#7363,#7364));
#1763=EDGE_LOOP('',(#7365,#7366,#7367,#7368));
#1764=EDGE_LOOP('',(#7369,#7370,#7371,#7372));
#1765=EDGE_LOOP('',(#7373,#7374,#7375,#7376,#7377,#7378,#7379,#7380,#7381,
#7382));
#1766=EDGE_LOOP('',(#7383));
#1767=EDGE_LOOP('',(#7384,#7385,#7386,#7387));
#1768=EDGE_LOOP('',(#7388));
#1769=EDGE_LOOP('',(#7389,#7390,#7391,#7392));
#1770=EDGE_LOOP('',(#7393,#7394,#7395,#7396));
#1771=EDGE_LOOP('',(#7397,#7398,#7399,#7400));
#1772=EDGE_LOOP('',(#7401));
#1773=EDGE_LOOP('',(#7402));
#1774=EDGE_LOOP('',(#7403,#7404,#7405,#7406));
#1775=EDGE_LOOP('',(#7407,#7408,#7409,#7410));
#1776=EDGE_LOOP('',(#7411));
#1777=EDGE_LOOP('',(#7412,#7413,#7414,#7415,#7416,#7417,#7418,#7419,#7420,
#7421,#7422,#7423));
#1778=EDGE_LOOP('',(#7424));
#1779=EDGE_LOOP('',(#7425,#7426,#7427,#7428,#7429));
#1780=EDGE_LOOP('',(#7430,#7431,#7432,#7433));
#2318=CIRCLE('',#10527,2.8);
#2319=CIRCLE('',#10530,17.85);
#2320=CIRCLE('',#10531,17.85);
#2321=CIRCLE('',#10532,17.85);
#2322=CIRCLE('',#10533,17.85);
#2323=CIRCLE('',#10535,20.);
#2324=CIRCLE('',#10536,15.);
#2325=CIRCLE('',#10538,20.);
#2326=CIRCLE('',#10539,20.);
#2327=CIRCLE('',#10541,19.5);
#2328=CIRCLE('',#10543,15.);
#2329=CIRCLE('',#10545,5.50000000000001);
#2330=CIRCLE('',#10546,3.);
#2331=CIRCLE('',#10548,17.85);
#2332=CIRCLE('',#10549,16.5);
#2333=CIRCLE('',#10551,16.5);
#2334=CIRCLE('',#10554,17.85);
#2335=CIRCLE('',#10557,3.);
#2336=CIRCLE('',#10559,5.);
#2337=CIRCLE('',#10560,5.);
#2338=CIRCLE('',#10561,5.);
#2339=CIRCLE('',#10562,5.);
#2340=CIRCLE('',#10565,3.);
#2341=CIRCLE('',#10570,3.);
#2342=CIRCLE('',#10573,2.8);
#2343=CIRCLE('',#10576,6.08697438789325);
#2897=LINE('',#17669,#3647);
#2898=LINE('',#17671,#3648);
#2899=LINE('',#17672,#3649);
#2900=LINE('',#17679,#3650);
#2901=LINE('',#17680,#3651);
#2902=LINE('',#17687,#3652);
#2903=LINE('',#17688,#3653);
#2904=LINE('',#17695,#3654);
#2905=LINE('',#17696,#3655);
#2906=LINE('',#17703,#3656);
#2907=LINE('',#17705,#3657);
#2908=LINE('',#17715,#3658);
#2909=LINE('',#17716,#3659);
#2910=LINE('',#17723,#3660);
#2911=LINE('',#17724,#3661);
#2912=LINE('',#17731,#3662);
#2913=LINE('',#17736,#3663);
#2914=LINE('',#17738,#3664);
#2915=LINE('',#17740,#3665);
#2916=LINE('',#17745,#3666);
#2917=LINE('',#17756,#3667);
#2918=LINE('',#17764,#3668);
#2919=LINE('',#17778,#3669);
#2920=LINE('',#17784,#3670);
#2921=LINE('',#17788,#3671);
#2922=LINE('',#17793,#3672);
#2923=LINE('',#17795,#3673);
#2924=LINE('',#17797,#3674);
#2925=LINE('',#17802,#3675);
#2926=LINE('',#17806,#3676);
#2927=LINE('',#17807,#3677);
#2928=LINE('',#17811,#3678);
#2929=LINE('',#17813,#3679);
#2930=LINE('',#17819,#3680);
#2931=LINE('',#17823,#3681);
#2932=LINE('',#17827,#3682);
#2933=LINE('',#17831,#3683);
#2934=LINE('',#17833,#3684);
#3647=VECTOR('',#12038,1000.);
#3648=VECTOR('',#12039,1000.);
#3649=VECTOR('',#12040,1000.);
#3650=VECTOR('',#12043,1000.);
#3651=VECTOR('',#12044,1000.);
#3652=VECTOR('',#12047,1000.);
#3653=VECTOR('',#12048,1000.);
#3654=VECTOR('',#12051,1000.);
#3655=VECTOR('',#12052,1000.);
#3656=VECTOR('',#12055,1000.);
#3657=VECTOR('',#12056,1000.);
#3658=VECTOR('',#12059,1000.);
#3659=VECTOR('',#12060,1000.);
#3660=VECTOR('',#12063,1000.);
#3661=VECTOR('',#12064,1000.);
#3662=VECTOR('',#12069,1000.);
#3663=VECTOR('',#12074,17.85);
#3664=VECTOR('',#12075,1000.);
#3665=VECTOR('',#12076,17.85);
#3666=VECTOR('',#12081,1000.);
#3667=VECTOR('',#12094,20.);
#3668=VECTOR('',#12105,15.);
#3669=VECTOR('',#12122,16.5);
#3670=VECTOR('',#12131,17.85);
#3671=VECTOR('',#12136,3.);
#3672=VECTOR('',#12141,5.);
#3673=VECTOR('',#12142,1000.);
#3674=VECTOR('',#12143,5.);
#3675=VECTOR('',#12148,1000.);
#3676=VECTOR('',#12155,1000.);
#3677=VECTOR('',#12156,1000.);
#3678=VECTOR('',#12161,1000.);
#3679=VECTOR('',#12164,1000.);
#3680=VECTOR('',#12173,3.);
#3681=VECTOR('',#12178,2.8);
#3682=VECTOR('',#12183,6.08697438789325);
#3683=VECTOR('',#12190,19.5);
#3684=VECTOR('',#12193,5.);
#4383=VERTEX_POINT('',#17663);
#4384=VERTEX_POINT('',#17664);
#4385=VERTEX_POINT('',#17668);
#4386=VERTEX_POINT('',#17670);
#4387=VERTEX_POINT('',#17674);
#4388=VERTEX_POINT('',#17678);
#4389=VERTEX_POINT('',#17682);
#4390=VERTEX_POINT('',#17686);
#4391=VERTEX_POINT('',#17690);
#4392=VERTEX_POINT('',#17694);
#4393=VERTEX_POINT('',#17698);
#4394=VERTEX_POINT('',#17702);
#4395=VERTEX_POINT('',#17704);
#4396=VERTEX_POINT('',#17710);
#4397=VERTEX_POINT('',#17714);
#4398=VERTEX_POINT('',#17718);
#4399=VERTEX_POINT('',#17722);
#4400=VERTEX_POINT('',#17725);
#4401=VERTEX_POINT('',#17733);
#4402=VERTEX_POINT('',#17735);
#4403=VERTEX_POINT('',#17737);
#4404=VERTEX_POINT('',#17739);
#4405=VERTEX_POINT('',#17742);
#4406=VERTEX_POINT('',#17744);
#4407=VERTEX_POINT('',#17748);
#4408=VERTEX_POINT('',#17750);
#4409=VERTEX_POINT('',#17753);
#4410=VERTEX_POINT('',#17754);
#4411=VERTEX_POINT('',#17759);
#4412=VERTEX_POINT('',#17762);
#4413=VERTEX_POINT('',#17766);
#4414=VERTEX_POINT('',#17768);
#4415=VERTEX_POINT('',#17771);
#4416=VERTEX_POINT('',#17773);
#4417=VERTEX_POINT('',#17776);
#4418=VERTEX_POINT('',#17781);
#4419=VERTEX_POINT('',#17786);
#4420=VERTEX_POINT('',#17790);
#4421=VERTEX_POINT('',#17792);
#4422=VERTEX_POINT('',#17794);
#4423=VERTEX_POINT('',#17796);
#4424=VERTEX_POINT('',#17799);
#4425=VERTEX_POINT('',#17801);
#4426=VERTEX_POINT('',#17808);
#4427=VERTEX_POINT('',#17816);
#4428=VERTEX_POINT('',#17821);
#4429=VERTEX_POINT('',#17826);
#5457=EDGE_CURVE('',#4383,#4384,#181,.T.);
#5458=EDGE_CURVE('',#4383,#4385,#2897,.T.);
#5459=EDGE_CURVE('',#4385,#4386,#2898,.T.);
#5460=EDGE_CURVE('',#4384,#4386,#2899,.T.);
#5461=EDGE_CURVE('',#4384,#4387,#182,.T.);
#5462=EDGE_CURVE('',#4386,#4388,#2900,.T.);
#5463=EDGE_CURVE('',#4387,#4388,#2901,.T.);
#5464=EDGE_CURVE('',#4387,#4389,#183,.T.);
#5465=EDGE_CURVE('',#4388,#4390,#2902,.T.);
#5466=EDGE_CURVE('',#4389,#4390,#2903,.T.);
#5467=EDGE_CURVE('',#4389,#4391,#184,.T.);
#5468=EDGE_CURVE('',#4390,#4392,#2904,.T.);
#5469=EDGE_CURVE('',#4391,#4392,#2905,.T.);
#5470=EDGE_CURVE('',#4391,#4393,#185,.T.);
#5471=EDGE_CURVE('',#4392,#4394,#2906,.T.);
#5472=EDGE_CURVE('',#4395,#4394,#2907,.T.);
#5473=EDGE_CURVE('',#4393,#4395,#186,.T.);
#5474=EDGE_CURVE('',#4395,#4396,#187,.T.);
#5475=EDGE_CURVE('',#4394,#4397,#2908,.T.);
#5476=EDGE_CURVE('',#4396,#4397,#2909,.T.);
#5477=EDGE_CURVE('',#4396,#4398,#188,.T.);
#5478=EDGE_CURVE('',#4397,#4399,#2910,.T.);
#5479=EDGE_CURVE('',#4398,#4399,#2911,.T.);
#5480=EDGE_CURVE('',#4400,#4400,#2318,.T.);
#5481=EDGE_CURVE('',#4398,#4383,#189,.T.);
#5482=EDGE_CURVE('',#4399,#4385,#2912,.T.);
#5483=EDGE_CURVE('',#4401,#4401,#2319,.T.);
#5484=EDGE_CURVE('',#4401,#4402,#2913,.T.);
#5485=EDGE_CURVE('',#4403,#4402,#2914,.T.);
#5486=EDGE_CURVE('',#4403,#4404,#2915,.T.);
#5487=EDGE_CURVE('',#4404,#4404,#2320,.T.);
#5488=EDGE_CURVE('',#4405,#4403,#2321,.T.);
#5489=EDGE_CURVE('',#4406,#4405,#2916,.T.);
#5490=EDGE_CURVE('',#4402,#4406,#2322,.T.);
#5491=EDGE_CURVE('',#4407,#4407,#2323,.T.);
#5492=EDGE_CURVE('',#4408,#4408,#2324,.T.);
#5493=EDGE_CURVE('',#4409,#4410,#2325,.T.);
#5494=EDGE_CURVE('',#4410,#4407,#2917,.T.);
#5495=EDGE_CURVE('',#4410,#4409,#2326,.T.);
#5496=EDGE_CURVE('',#4411,#4411,#2327,.T.);
#5497=EDGE_CURVE('',#4412,#4412,#2328,.T.);
#5498=EDGE_CURVE('',#4412,#4408,#2918,.T.);
#5499=EDGE_CURVE('',#4413,#4413,#2329,.T.);
#5500=EDGE_CURVE('',#4414,#4414,#2330,.T.);
#5501=EDGE_CURVE('',#4415,#4415,#2331,.T.);
#5502=EDGE_CURVE('',#4416,#4416,#2332,.T.);
#5503=EDGE_CURVE('',#4417,#4417,#2333,.T.);
#5504=EDGE_CURVE('',#4417,#4416,#2919,.T.);
#5505=EDGE_CURVE('',#4418,#4418,#2334,.T.);
#5506=EDGE_CURVE('',#4418,#4415,#2920,.T.);
#5507=EDGE_CURVE('',#4419,#4419,#2335,.T.);
#5508=EDGE_CURVE('',#4419,#4414,#2921,.T.);
#5509=EDGE_CURVE('',#4420,#4420,#2336,.T.);
#5510=EDGE_CURVE('',#4420,#4421,#2922,.T.);
#5511=EDGE_CURVE('',#4421,#4422,#2923,.T.);
#5512=EDGE_CURVE('',#4422,#4423,#2924,.T.);
#5513=EDGE_CURVE('',#4423,#4423,#2337,.T.);
#5514=EDGE_CURVE('',#4422,#4424,#2338,.T.);
#5515=EDGE_CURVE('',#4424,#4425,#2925,.T.);
#5516=EDGE_CURVE('',#4425,#4421,#2339,.T.);
#5517=EDGE_CURVE('',#4406,#4421,#2926,.T.);
#5518=EDGE_CURVE('',#4425,#4402,#2927,.T.);
#5519=EDGE_CURVE('',#4426,#4426,#2340,.T.);
#5520=EDGE_CURVE('',#4424,#4403,#2928,.T.);
#5521=EDGE_CURVE('',#4405,#4422,#2929,.T.);
#5522=EDGE_CURVE('',#4427,#4427,#2341,.T.);
#5523=EDGE_CURVE('',#4427,#4426,#2930,.T.);
#5524=EDGE_CURVE('',#4428,#4428,#2342,.T.);
#5525=EDGE_CURVE('',#4428,#4400,#2931,.T.);
#5526=EDGE_CURVE('',#4393,#4429,#2932,.T.);
#5527=EDGE_CURVE('',#4429,#4429,#2343,.T.);
#5528=EDGE_CURVE('',#4409,#4411,#2933,.T.);
#5529=EDGE_CURVE('',#4423,#4413,#2934,.T.);
#7288=ORIENTED_EDGE('',*,*,#5457,.F.);
#7289=ORIENTED_EDGE('',*,*,#5458,.T.);
#7290=ORIENTED_EDGE('',*,*,#5459,.T.);
#7291=ORIENTED_EDGE('',*,*,#5460,.F.);
#7292=ORIENTED_EDGE('',*,*,#5461,.F.);
#7293=ORIENTED_EDGE('',*,*,#5460,.T.);
#7294=ORIENTED_EDGE('',*,*,#5462,.T.);
#7295=ORIENTED_EDGE('',*,*,#5463,.F.);
#7296=ORIENTED_EDGE('',*,*,#5464,.F.);
#7297=ORIENTED_EDGE('',*,*,#5463,.T.);
#7298=ORIENTED_EDGE('',*,*,#5465,.T.);
#7299=ORIENTED_EDGE('',*,*,#5466,.F.);
#7300=ORIENTED_EDGE('',*,*,#5467,.F.);
#7301=ORIENTED_EDGE('',*,*,#5466,.T.);
#7302=ORIENTED_EDGE('',*,*,#5468,.T.);
#7303=ORIENTED_EDGE('',*,*,#5469,.F.);
#7304=ORIENTED_EDGE('',*,*,#5470,.F.);
#7305=ORIENTED_EDGE('',*,*,#5469,.T.);
#7306=ORIENTED_EDGE('',*,*,#5471,.T.);
#7307=ORIENTED_EDGE('',*,*,#5472,.F.);
#7308=ORIENTED_EDGE('',*,*,#5473,.F.);
#7309=ORIENTED_EDGE('',*,*,#5474,.F.);
#7310=ORIENTED_EDGE('',*,*,#5472,.T.);
#7311=ORIENTED_EDGE('',*,*,#5475,.T.);
#7312=ORIENTED_EDGE('',*,*,#5476,.F.);
#7313=ORIENTED_EDGE('',*,*,#5477,.F.);
#7314=ORIENTED_EDGE('',*,*,#5476,.T.);
#7315=ORIENTED_EDGE('',*,*,#5478,.T.);
#7316=ORIENTED_EDGE('',*,*,#5479,.F.);
#7317=ORIENTED_EDGE('',*,*,#5480,.F.);
#7318=ORIENTED_EDGE('',*,*,#5481,.F.);
#7319=ORIENTED_EDGE('',*,*,#5479,.T.);
#7320=ORIENTED_EDGE('',*,*,#5482,.T.);
#7321=ORIENTED_EDGE('',*,*,#5458,.F.);
#7322=ORIENTED_EDGE('',*,*,#5483,.T.);
#7323=ORIENTED_EDGE('',*,*,#5484,.T.);
#7324=ORIENTED_EDGE('',*,*,#5485,.F.);
#7325=ORIENTED_EDGE('',*,*,#5486,.T.);
#7326=ORIENTED_EDGE('',*,*,#5487,.T.);
#7327=ORIENTED_EDGE('',*,*,#5486,.F.);
#7328=ORIENTED_EDGE('',*,*,#5488,.F.);
#7329=ORIENTED_EDGE('',*,*,#5489,.F.);
#7330=ORIENTED_EDGE('',*,*,#5490,.F.);
#7331=ORIENTED_EDGE('',*,*,#5484,.F.);
#7332=ORIENTED_EDGE('',*,*,#5491,.F.);
#7333=ORIENTED_EDGE('',*,*,#5492,.F.);
#7334=ORIENTED_EDGE('',*,*,#5493,.T.);
#7335=ORIENTED_EDGE('',*,*,#5494,.T.);
#7336=ORIENTED_EDGE('',*,*,#5491,.T.);
#7337=ORIENTED_EDGE('',*,*,#5494,.F.);
#7338=ORIENTED_EDGE('',*,*,#5495,.T.);
#7339=ORIENTED_EDGE('',*,*,#5496,.T.);
#7340=ORIENTED_EDGE('',*,*,#5487,.F.);
#7341=ORIENTED_EDGE('',*,*,#5497,.F.);
#7342=ORIENTED_EDGE('',*,*,#5498,.T.);
#7343=ORIENTED_EDGE('',*,*,#5492,.T.);
#7344=ORIENTED_EDGE('',*,*,#5498,.F.);
#7345=ORIENTED_EDGE('',*,*,#5497,.T.);
#7346=ORIENTED_EDGE('',*,*,#5499,.T.);
#7347=ORIENTED_EDGE('',*,*,#5500,.F.);
#7348=ORIENTED_EDGE('',*,*,#5501,.T.);
#7349=ORIENTED_EDGE('',*,*,#5502,.F.);
#7350=ORIENTED_EDGE('',*,*,#5503,.F.);
#7351=ORIENTED_EDGE('',*,*,#5504,.T.);
#7352=ORIENTED_EDGE('',*,*,#5502,.T.);
#7353=ORIENTED_EDGE('',*,*,#5504,.F.);
#7354=ORIENTED_EDGE('',*,*,#5483,.F.);
#7355=ORIENTED_EDGE('',*,*,#5503,.T.);
#7356=ORIENTED_EDGE('',*,*,#5505,.T.);
#7357=ORIENTED_EDGE('',*,*,#5459,.F.);
#7358=ORIENTED_EDGE('',*,*,#5482,.F.);
#7359=ORIENTED_EDGE('',*,*,#5478,.F.);
#7360=ORIENTED_EDGE('',*,*,#5475,.F.);
#7361=ORIENTED_EDGE('',*,*,#5471,.F.);
#7362=ORIENTED_EDGE('',*,*,#5468,.F.);
#7363=ORIENTED_EDGE('',*,*,#5465,.F.);
#7364=ORIENTED_EDGE('',*,*,#5462,.F.);
#7365=ORIENTED_EDGE('',*,*,#5505,.F.);
#7366=ORIENTED_EDGE('',*,*,#5506,.T.);
#7367=ORIENTED_EDGE('',*,*,#5501,.F.);
#7368=ORIENTED_EDGE('',*,*,#5506,.F.);
#7369=ORIENTED_EDGE('',*,*,#5507,.T.);
#7370=ORIENTED_EDGE('',*,*,#5508,.T.);
#7371=ORIENTED_EDGE('',*,*,#5500,.T.);
#7372=ORIENTED_EDGE('',*,*,#5508,.F.);
#7373=ORIENTED_EDGE('',*,*,#5509,.F.);
#7374=ORIENTED_EDGE('',*,*,#5510,.T.);
#7375=ORIENTED_EDGE('',*,*,#5511,.T.);
#7376=ORIENTED_EDGE('',*,*,#5512,.T.);
#7377=ORIENTED_EDGE('',*,*,#5513,.T.);
#7378=ORIENTED_EDGE('',*,*,#5512,.F.);
#7379=ORIENTED_EDGE('',*,*,#5514,.T.);
#7380=ORIENTED_EDGE('',*,*,#5515,.T.);
#7381=ORIENTED_EDGE('',*,*,#5516,.T.);
#7382=ORIENTED_EDGE('',*,*,#5510,.F.);
#7383=ORIENTED_EDGE('',*,*,#5509,.T.);
#7384=ORIENTED_EDGE('',*,*,#5490,.T.);
#7385=ORIENTED_EDGE('',*,*,#5517,.T.);
#7386=ORIENTED_EDGE('',*,*,#5516,.F.);
#7387=ORIENTED_EDGE('',*,*,#5518,.T.);
#7388=ORIENTED_EDGE('',*,*,#5519,.F.);
#7389=ORIENTED_EDGE('',*,*,#5485,.T.);
#7390=ORIENTED_EDGE('',*,*,#5518,.F.);
#7391=ORIENTED_EDGE('',*,*,#5515,.F.);
#7392=ORIENTED_EDGE('',*,*,#5520,.T.);
#7393=ORIENTED_EDGE('',*,*,#5489,.T.);
#7394=ORIENTED_EDGE('',*,*,#5521,.T.);
#7395=ORIENTED_EDGE('',*,*,#5511,.F.);
#7396=ORIENTED_EDGE('',*,*,#5517,.F.);
#7397=ORIENTED_EDGE('',*,*,#5488,.T.);
#7398=ORIENTED_EDGE('',*,*,#5520,.F.);
#7399=ORIENTED_EDGE('',*,*,#5514,.F.);
#7400=ORIENTED_EDGE('',*,*,#5521,.F.);
#7401=ORIENTED_EDGE('',*,*,#5507,.F.);
#7402=ORIENTED_EDGE('',*,*,#5522,.T.);
#7403=ORIENTED_EDGE('',*,*,#5522,.F.);
#7404=ORIENTED_EDGE('',*,*,#5523,.T.);
#7405=ORIENTED_EDGE('',*,*,#5519,.T.);
#7406=ORIENTED_EDGE('',*,*,#5523,.F.);
#7407=ORIENTED_EDGE('',*,*,#5524,.F.);
#7408=ORIENTED_EDGE('',*,*,#5525,.T.);
#7409=ORIENTED_EDGE('',*,*,#5480,.T.);
#7410=ORIENTED_EDGE('',*,*,#5525,.F.);
#7411=ORIENTED_EDGE('',*,*,#5524,.T.);
#7412=ORIENTED_EDGE('',*,*,#5457,.T.);
#7413=ORIENTED_EDGE('',*,*,#5461,.T.);
#7414=ORIENTED_EDGE('',*,*,#5464,.T.);
#7415=ORIENTED_EDGE('',*,*,#5467,.T.);
#7416=ORIENTED_EDGE('',*,*,#5470,.T.);
#7417=ORIENTED_EDGE('',*,*,#5526,.T.);
#7418=ORIENTED_EDGE('',*,*,#5527,.F.);
#7419=ORIENTED_EDGE('',*,*,#5526,.F.);
#7420=ORIENTED_EDGE('',*,*,#5473,.T.);
#7421=ORIENTED_EDGE('',*,*,#5474,.T.);
#7422=ORIENTED_EDGE('',*,*,#5477,.T.);
#7423=ORIENTED_EDGE('',*,*,#5481,.T.);
#7424=ORIENTED_EDGE('',*,*,#5527,.T.);
#7425=ORIENTED_EDGE('',*,*,#5493,.F.);
#7426=ORIENTED_EDGE('',*,*,#5528,.T.);
#7427=ORIENTED_EDGE('',*,*,#5496,.F.);
#7428=ORIENTED_EDGE('',*,*,#5528,.F.);
#7429=ORIENTED_EDGE('',*,*,#5495,.F.);
#7430=ORIENTED_EDGE('',*,*,#5513,.F.);
#7431=ORIENTED_EDGE('',*,*,#5529,.T.);
#7432=ORIENTED_EDGE('',*,*,#5499,.F.);
#7433=ORIENTED_EDGE('',*,*,#5529,.F.);
#9267=CYLINDRICAL_SURFACE('',#10529,17.85);
#9268=CYLINDRICAL_SURFACE('',#10537,20.);
#9269=CYLINDRICAL_SURFACE('',#10542,15.);
#9270=CYLINDRICAL_SURFACE('',#10550,16.5);
#9271=CYLINDRICAL_SURFACE('',#10555,17.85);
#9272=CYLINDRICAL_SURFACE('',#10556,3.);
#9273=CYLINDRICAL_SURFACE('',#10558,5.);
#9274=CYLINDRICAL_SURFACE('',#10571,3.);
#9275=CYLINDRICAL_SURFACE('',#10572,2.8);
#9540=ADVANCED_FACE('',(#1174),#843,.F.);
#9541=ADVANCED_FACE('',(#1175),#844,.F.);
#9542=ADVANCED_FACE('',(#1176),#845,.F.);
#9543=ADVANCED_FACE('',(#1177),#846,.F.);
#9544=ADVANCED_FACE('',(#1178),#847,.F.);
#9545=ADVANCED_FACE('',(#1179),#848,.F.);
#9546=ADVANCED_FACE('',(#1180,#481),#849,.F.);
#9547=ADVANCED_FACE('',(#1181),#850,.F.);
#9548=ADVANCED_FACE('',(#1182),#9267,.T.);
#9549=ADVANCED_FACE('',(#1183,#482),#851,.T.);
#9550=ADVANCED_FACE('',(#1184),#9268,.T.);
#9551=ADVANCED_FACE('',(#1185,#483),#852,.T.);
#9552=ADVANCED_FACE('',(#1186),#9269,.F.);
#9553=ADVANCED_FACE('',(#1187,#484,#485),#853,.T.);
#9554=ADVANCED_FACE('',(#1188,#486),#854,.T.);
#9555=ADVANCED_FACE('',(#1189),#9270,.T.);
#9556=ADVANCED_FACE('',(#1190,#487),#855,.T.);
#9557=ADVANCED_FACE('',(#1191,#488),#856,.T.);
#9558=ADVANCED_FACE('',(#1192),#9271,.T.);
#9559=ADVANCED_FACE('',(#1193),#9272,.F.);
#9560=ADVANCED_FACE('',(#1194),#9273,.F.);
#9561=ADVANCED_FACE('',(#1195),#857,.T.);
#9562=ADVANCED_FACE('',(#1196,#489),#858,.F.);
#9563=ADVANCED_FACE('',(#1197),#859,.F.);
#9564=ADVANCED_FACE('',(#1198),#860,.F.);
#9565=ADVANCED_FACE('',(#1199,#490),#861,.F.);
#9566=ADVANCED_FACE('',(#1200),#862,.T.);
#9567=ADVANCED_FACE('',(#1201),#9274,.F.);
#9568=ADVANCED_FACE('',(#1202),#9275,.F.);
#9569=ADVANCED_FACE('',(#1203),#863,.T.);
#9570=ADVANCED_FACE('',(#1204),#346,.T.);
#9571=ADVANCED_FACE('',(#1205),#864,.F.);
#9572=ADVANCED_FACE('',(#1206),#347,.T.);
#9573=ADVANCED_FACE('',(#1207),#348,.F.);
#9943=CLOSED_SHELL('',(#9540,#9541,#9542,#9543,#9544,#9545,#9546,#9547,
#9548,#9549,#9550,#9551,#9552,#9553,#9554,#9555,#9556,#9557,#9558,#9559,
#9560,#9561,#9562,#9563,#9564,#9565,#9566,#9567,#9568,#9569,#9570,#9571,
#9572,#9573));
#10519=AXIS2_PLACEMENT_3D('',#17661,#12034,#12035);
#10520=AXIS2_PLACEMENT_3D('',#17662,#12036,#12037);
#10521=AXIS2_PLACEMENT_3D('',#17673,#12041,#12042);
#10522=AXIS2_PLACEMENT_3D('',#17681,#12045,#12046);
#10523=AXIS2_PLACEMENT_3D('',#17689,#12049,#12050);
#10524=AXIS2_PLACEMENT_3D('',#17697,#12053,#12054);
#10525=AXIS2_PLACEMENT_3D('',#17709,#12057,#12058);
#10526=AXIS2_PLACEMENT_3D('',#17717,#12061,#12062);
#10527=AXIS2_PLACEMENT_3D('',#17726,#12065,#12066);
#10528=AXIS2_PLACEMENT_3D('',#17727,#12067,#12068);
#10529=AXIS2_PLACEMENT_3D('',#17732,#12070,#12071);
#10530=AXIS2_PLACEMENT_3D('',#17734,#12072,#12073);
#10531=AXIS2_PLACEMENT_3D('',#17741,#12077,#12078);
#10532=AXIS2_PLACEMENT_3D('',#17743,#12079,#12080);
#10533=AXIS2_PLACEMENT_3D('',#17746,#12082,#12083);
#10534=AXIS2_PLACEMENT_3D('',#17747,#12084,#12085);
#10535=AXIS2_PLACEMENT_3D('',#17749,#12086,#12087);
#10536=AXIS2_PLACEMENT_3D('',#17751,#12088,#12089);
#10537=AXIS2_PLACEMENT_3D('',#17752,#12090,#12091);
#10538=AXIS2_PLACEMENT_3D('',#17755,#12092,#12093);
#10539=AXIS2_PLACEMENT_3D('',#17757,#12095,#12096);
#10540=AXIS2_PLACEMENT_3D('',#17758,#12097,#12098);
#10541=AXIS2_PLACEMENT_3D('',#17760,#12099,#12100);
#10542=AXIS2_PLACEMENT_3D('',#17761,#12101,#12102);
#10543=AXIS2_PLACEMENT_3D('',#17763,#12103,#12104);
#10544=AXIS2_PLACEMENT_3D('',#17765,#12106,#12107);
#10545=AXIS2_PLACEMENT_3D('',#17767,#12108,#12109);
#10546=AXIS2_PLACEMENT_3D('',#17769,#12110,#12111);
#10547=AXIS2_PLACEMENT_3D('',#17770,#12112,#12113);
#10548=AXIS2_PLACEMENT_3D('',#17772,#12114,#12115);
#10549=AXIS2_PLACEMENT_3D('',#17774,#12116,#12117);
#10550=AXIS2_PLACEMENT_3D('',#17775,#12118,#12119);
#10551=AXIS2_PLACEMENT_3D('',#17777,#12120,#12121);
#10552=AXIS2_PLACEMENT_3D('',#17779,#12123,#12124);
#10553=AXIS2_PLACEMENT_3D('',#17780,#12125,#12126);
#10554=AXIS2_PLACEMENT_3D('',#17782,#12127,#12128);
#10555=AXIS2_PLACEMENT_3D('',#17783,#12129,#12130);
#10556=AXIS2_PLACEMENT_3D('',#17785,#12132,#12133);
#10557=AXIS2_PLACEMENT_3D('',#17787,#12134,#12135);
#10558=AXIS2_PLACEMENT_3D('',#17789,#12137,#12138);
#10559=AXIS2_PLACEMENT_3D('',#17791,#12139,#12140);
#10560=AXIS2_PLACEMENT_3D('',#17798,#12144,#12145);
#10561=AXIS2_PLACEMENT_3D('',#17800,#12146,#12147);
#10562=AXIS2_PLACEMENT_3D('',#17803,#12149,#12150);
#10563=AXIS2_PLACEMENT_3D('',#17804,#12151,#12152);
#10564=AXIS2_PLACEMENT_3D('',#17805,#12153,#12154);
#10565=AXIS2_PLACEMENT_3D('',#17809,#12157,#12158);
#10566=AXIS2_PLACEMENT_3D('',#17810,#12159,#12160);
#10567=AXIS2_PLACEMENT_3D('',#17812,#12162,#12163);
#10568=AXIS2_PLACEMENT_3D('',#17814,#12165,#12166);
#10569=AXIS2_PLACEMENT_3D('',#17815,#12167,#12168);
#10570=AXIS2_PLACEMENT_3D('',#17817,#12169,#12170);
#10571=AXIS2_PLACEMENT_3D('',#17818,#12171,#12172);
#10572=AXIS2_PLACEMENT_3D('',#17820,#12174,#12175);
#10573=AXIS2_PLACEMENT_3D('',#17822,#12176,#12177);
#10574=AXIS2_PLACEMENT_3D('',#17824,#12179,#12180);
#10575=AXIS2_PLACEMENT_3D('',#17825,#12181,#12182);
#10576=AXIS2_PLACEMENT_3D('',#17828,#12184,#12185);
#10577=AXIS2_PLACEMENT_3D('',#17829,#12186,#12187);
#10578=AXIS2_PLACEMENT_3D('',#17830,#12188,#12189);
#10579=AXIS2_PLACEMENT_3D('',#17832,#12191,#12192);
#12034=DIRECTION('axis',(0.,0.,1.));
#12035=DIRECTION('refdir',(1.,0.,0.));
#12036=DIRECTION('center_axis',(-7.74415657941891E-17,0.,-1.));
#12037=DIRECTION('ref_axis',(-1.,0.,7.74415657941892E-17));
#12038=DIRECTION('',(0.,1.,0.));
#12039=DIRECTION('',(-1.,0.,7.74415657941891E-17));
#12040=DIRECTION('',(0.,1.,0.));
#12041=DIRECTION('center_axis',(0.707106781186548,0.,-0.707106781186547));
#12042=DIRECTION('ref_axis',(-0.707106781186547,0.,-0.707106781186548));
#12043=DIRECTION('',(-0.707106781186547,0.,-0.707106781186548));
#12044=DIRECTION('',(0.,1.,0.));
#12045=DIRECTION('center_axis',(1.,0.,-7.74415657941891E-17));
#12046=DIRECTION('ref_axis',(-7.74415657941891E-17,0.,-1.));
#12047=DIRECTION('',(-7.74415657941891E-17,0.,-1.));
#12048=DIRECTION('',(0.,1.,0.));
#12049=DIRECTION('center_axis',(0.707106781186547,0.,0.707106781186548));
#12050=DIRECTION('ref_axis',(0.707106781186548,0.,-0.707106781186547));
#12051=DIRECTION('',(0.707106781186548,0.,-0.707106781186547));
#12052=DIRECTION('',(0.,1.,0.));
#12053=DIRECTION('center_axis',(0.,0.,1.));
#12054=DIRECTION('ref_axis',(1.,0.,0.));
#12055=DIRECTION('',(1.,0.,0.));
#12056=DIRECTION('',(0.,1.,0.));
#12057=DIRECTION('center_axis',(-0.707106781186547,0.,0.707106781186548));
#12058=DIRECTION('ref_axis',(0.707106781186548,0.,0.707106781186547));
#12059=DIRECTION('',(0.707106781186548,0.,0.707106781186547));
#12060=DIRECTION('',(0.,1.,0.));
#12061=DIRECTION('center_axis',(-1.,0.,0.));
#12062=DIRECTION('ref_axis',(0.,0.,1.));
#12063=DIRECTION('',(0.,0.,1.));
#12064=DIRECTION('',(0.,1.,0.));
#12065=DIRECTION('center_axis',(1.,0.,1.36592399683213E-16));
#12066=DIRECTION('ref_axis',(1.36592399683213E-16,0.,-1.));
#12067=DIRECTION('center_axis',(-0.707106781186547,0.,-0.707106781186548));
#12068=DIRECTION('ref_axis',(-0.707106781186548,0.,0.707106781186547));
#12069=DIRECTION('',(-0.707106781186548,0.,0.707106781186547));
#12070=DIRECTION('center_axis',(0.,-1.,0.));
#12071=DIRECTION('ref_axis',(0.,0.,-1.));
#12072=DIRECTION('center_axis',(0.,1.,0.));
#12073=DIRECTION('ref_axis',(0.,0.,1.));
#12074=DIRECTION('',(0.,1.,0.));
#12075=DIRECTION('',(0.,-1.,0.));
#12076=DIRECTION('',(0.,1.,0.));
#12077=DIRECTION('center_axis',(0.,-1.,0.));
#12078=DIRECTION('ref_axis',(0.,0.,-1.));
#12079=DIRECTION('center_axis',(1.9436677601981E-16,-1.,0.));
#12080=DIRECTION('ref_axis',(-1.,-1.9436677601981E-16,0.));
#12081=DIRECTION('',(0.,1.,0.));
#12082=DIRECTION('center_axis',(-9.71833880099051E-17,1.,0.));
#12083=DIRECTION('ref_axis',(1.,9.71833880099051E-17,0.));
#12084=DIRECTION('center_axis',(0.,1.,0.));
#12085=DIRECTION('ref_axis',(0.,0.,1.));
#12086=DIRECTION('center_axis',(0.,-1.,0.));
#12087=DIRECTION('ref_axis',(0.,0.,-1.));
#12088=DIRECTION('center_axis',(0.,1.,0.));
#12089=DIRECTION('ref_axis',(0.,0.,1.));
#12090=DIRECTION('center_axis',(0.,-1.,0.));
#12091=DIRECTION('ref_axis',(0.,0.,-1.));
#12092=DIRECTION('center_axis',(0.,1.,0.));
#12093=DIRECTION('ref_axis',(0.,0.,-1.));
#12094=DIRECTION('',(0.,1.,0.));
#12095=DIRECTION('center_axis',(0.,1.,0.));
#12096=DIRECTION('ref_axis',(0.,0.,-1.));
#12097=DIRECTION('center_axis',(0.,-1.,0.));
#12098=DIRECTION('ref_axis',(0.,0.,-1.));
#12099=DIRECTION('center_axis',(0.,-1.,0.));
#12100=DIRECTION('ref_axis',(0.,0.,-1.));
#12101=DIRECTION('center_axis',(0.,1.,0.));
#12102=DIRECTION('ref_axis',(0.,0.,1.));
#12103=DIRECTION('center_axis',(0.,1.,0.));
#12104=DIRECTION('ref_axis',(0.,0.,1.));
#12105=DIRECTION('',(0.,1.,0.));
#12106=DIRECTION('center_axis',(0.,1.,0.));
#12107=DIRECTION('ref_axis',(0.,0.,1.));
#12108=DIRECTION('center_axis',(0.,-1.,0.));
#12109=DIRECTION('ref_axis',(0.,0.,1.));
#12110=DIRECTION('center_axis',(0.,1.,0.));
#12111=DIRECTION('ref_axis',(0.,0.,1.));
#12112=DIRECTION('center_axis',(0.,1.,0.));
#12113=DIRECTION('ref_axis',(0.,0.,1.));
#12114=DIRECTION('center_axis',(0.,1.,0.));
#12115=DIRECTION('ref_axis',(0.,0.,1.));
#12116=DIRECTION('center_axis',(0.,1.,0.));
#12117=DIRECTION('ref_axis',(0.,0.,1.));
#12118=DIRECTION('center_axis',(0.,1.,0.));
#12119=DIRECTION('ref_axis',(0.,0.,1.));
#12120=DIRECTION('center_axis',(0.,1.,0.));
#12121=DIRECTION('ref_axis',(0.,0.,1.));
#12122=DIRECTION('',(0.,-1.,0.));
#12123=DIRECTION('center_axis',(0.,-1.,0.));
#12124=DIRECTION('ref_axis',(0.,0.,-1.));
#12125=DIRECTION('center_axis',(0.,-1.,0.));
#12126=DIRECTION('ref_axis',(0.,0.,-1.));
#12127=DIRECTION('center_axis',(0.,-1.,0.));
#12128=DIRECTION('ref_axis',(0.,0.,-1.));
#12129=DIRECTION('center_axis',(0.,-1.,0.));
#12130=DIRECTION('ref_axis',(0.,0.,-1.));
#12131=DIRECTION('',(0.,1.,0.));
#12132=DIRECTION('center_axis',(0.,1.,0.));
#12133=DIRECTION('ref_axis',(0.,0.,1.));
#12134=DIRECTION('center_axis',(1.9436677601981E-16,-1.,0.));
#12135=DIRECTION('ref_axis',(-1.,-1.9436677601981E-16,0.));
#12136=DIRECTION('',(0.,1.,0.));
#12137=DIRECTION('center_axis',(0.,1.,0.));
#12138=DIRECTION('ref_axis',(0.,0.,1.));
#12139=DIRECTION('center_axis',(0.,1.,0.));
#12140=DIRECTION('ref_axis',(0.,0.,1.));
#12141=DIRECTION('',(0.,1.,0.));
#12142=DIRECTION('',(0.,1.,0.));
#12143=DIRECTION('',(0.,1.,0.));
#12144=DIRECTION('center_axis',(0.,1.,0.));
#12145=DIRECTION('ref_axis',(0.,0.,1.));
#12146=DIRECTION('center_axis',(1.9436677601981E-16,-1.,0.));
#12147=DIRECTION('ref_axis',(-1.,-1.9436677601981E-16,0.));
#12148=DIRECTION('',(0.,-1.,0.));
#12149=DIRECTION('center_axis',(-9.71833880099051E-17,1.,0.));
#12150=DIRECTION('ref_axis',(1.,9.71833880099052E-17,0.));
#12151=DIRECTION('center_axis',(0.,1.,0.));
#12152=DIRECTION('ref_axis',(0.,0.,1.));
#12153=DIRECTION('center_axis',(9.71833880099051E-17,-1.,0.));
#12154=DIRECTION('ref_axis',(1.,9.71833880099052E-17,0.));
#12155=DIRECTION('',(0.,0.,1.));
#12156=DIRECTION('',(0.,0.,1.));
#12157=DIRECTION('center_axis',(-9.71833880099051E-17,1.,0.));
#12158=DIRECTION('ref_axis',(1.,9.71833880099052E-17,0.));
#12159=DIRECTION('center_axis',(-1.,-8.41343455666662E-18,0.));
#12160=DIRECTION('ref_axis',(8.41343455666662E-18,-1.,0.));
#12161=DIRECTION('',(0.,0.,1.));
#12162=DIRECTION('center_axis',(-1.,-8.41343455666662E-18,0.));
#12163=DIRECTION('ref_axis',(8.41343455666662E-18,-1.,0.));
#12164=DIRECTION('',(0.,0.,1.));
#12165=DIRECTION('center_axis',(-1.9436677601981E-16,1.,0.));
#12166=DIRECTION('ref_axis',(-1.,-1.9436677601981E-16,0.));
#12167=DIRECTION('center_axis',(0.,1.,0.));
#12168=DIRECTION('ref_axis',(0.,0.,1.));
#12169=DIRECTION('center_axis',(0.,1.,0.));
#12170=DIRECTION('ref_axis',(0.,0.,1.));
#12171=DIRECTION('center_axis',(0.,1.,0.));
#12172=DIRECTION('ref_axis',(0.,0.,1.));
#12173=DIRECTION('',(0.,1.,0.));
#12174=DIRECTION('center_axis',(1.,0.,1.36592399683213E-16));
#12175=DIRECTION('ref_axis',(1.36592399683213E-16,0.,-1.));
#12176=DIRECTION('center_axis',(1.,0.,1.36592399683213E-16));
#12177=DIRECTION('ref_axis',(1.36592399683213E-16,0.,-1.));
#12178=DIRECTION('',(1.,0.,1.36592399683213E-16));
#12179=DIRECTION('center_axis',(1.,0.,1.36592399683213E-16));
#12180=DIRECTION('ref_axis',(1.36592399683213E-16,0.,-1.));
#12181=DIRECTION('center_axis',(0.,1.,0.));
#12182=DIRECTION('ref_axis',(0.,0.,1.));
#12183=DIRECTION('',(1.10990693043676E-16,-0.422618261740693,0.906307787036653));
#12184=DIRECTION('center_axis',(0.,-1.,0.));
#12185=DIRECTION('ref_axis',(0.,0.,-1.));
#12186=DIRECTION('center_axis',(0.,1.,0.));
#12187=DIRECTION('ref_axis',(0.,0.,1.));
#12188=DIRECTION('center_axis',(0.,1.,0.));
#12189=DIRECTION('ref_axis',(0.,0.,1.));
#12190=DIRECTION('',(8.65956056235481E-17,-0.707106781186557,0.707106781186538));
#12191=DIRECTION('center_axis',(0.,1.,0.));
#12192=DIRECTION('ref_axis',(0.,0.,1.));
#12193=DIRECTION('',(-8.65956056235497E-17,0.707106781186544,-0.707106781186551));
#17661=CARTESIAN_POINT('',(0.,0.,0.));
#17662=CARTESIAN_POINT('Origin',(-5.60010460205265,-15.5,6.34999999999999));
#17663=CARTESIAN_POINT('',(5.60010460205265,-14.390352550159,6.34999999999999));
#17664=CARTESIAN_POINT('',(-5.60010460205265,-14.390352550159,6.34999999999999));
#17665=CARTESIAN_POINT('Ctrl Pts',(5.6001046019848,-14.3903525501799,6.35));
#17666=CARTESIAN_POINT('Ctrl Pts',(-2.66453525910038E-15,-16.1176005778891,
6.35));
#17667=CARTESIAN_POINT('Ctrl Pts',(-5.60010460198481,-14.3903525501799,
6.35));
#17668=CARTESIAN_POINT('',(5.60010460205265,0.,6.34999999999999));
#17669=CARTESIAN_POINT('',(5.60010460205265,-15.5,6.34999999999999));
#17670=CARTESIAN_POINT('',(-5.60010460205265,0.,6.34999999999999));
#17671=CARTESIAN_POINT('',(-5.60010460205265,0.,6.34999999999999));
#17672=CARTESIAN_POINT('',(-5.60010460205265,-15.5,6.34999999999999));
#17673=CARTESIAN_POINT('Origin',(-6.35,-15.5,5.60010460205265));
#17674=CARTESIAN_POINT('',(-6.35,-14.390352550159,5.60010460205265));
#17675=CARTESIAN_POINT('Ctrl Pts',(-5.60010460206764,-14.3903525501596,
6.349999999985));
#17676=CARTESIAN_POINT('Ctrl Pts',(-5.97505230102632,-14.4058383559469,
5.97505230102632));
#17677=CARTESIAN_POINT('Ctrl Pts',(-6.34999999998501,-14.3903525501596,
5.60010460206763));
#17678=CARTESIAN_POINT('',(-6.35,0.,5.60010460205265));
#17679=CARTESIAN_POINT('',(-6.35,0.,5.60010460205265));
#17680=CARTESIAN_POINT('',(-6.35,-15.5,5.60010460205265));
#17681=CARTESIAN_POINT('Origin',(-6.35,-15.5,5.60010460205265));
#17682=CARTESIAN_POINT('',(-6.35,-14.390352550159,-5.60010460205265));
#17683=CARTESIAN_POINT('Ctrl Pts',(-6.35,-14.3903525501799,5.60010460198479));
#17684=CARTESIAN_POINT('Ctrl Pts',(-6.35,-16.1176005778891,-1.46549439250521E-14));
#17685=CARTESIAN_POINT('Ctrl Pts',(-6.35,-14.3903525501799,-5.60010460198484));
#17686=CARTESIAN_POINT('',(-6.35,0.,-5.60010460205265));
#17687=CARTESIAN_POINT('',(-6.35,0.,5.60010460205265));
#17688=CARTESIAN_POINT('',(-6.35,-15.5,-5.60010460205265));
#17689=CARTESIAN_POINT('Origin',(-6.35,-15.5,-5.60010460205265));
#17690=CARTESIAN_POINT('',(-5.60010460205266,-14.390352550159,-6.34999999999999));
#17691=CARTESIAN_POINT('Ctrl Pts',(-6.34999999998502,-14.3903525501596,
-5.60010460206762));
#17692=CARTESIAN_POINT('Ctrl Pts',(-5.97505230102633,-14.4058383559469,
-5.97505230102631));
#17693=CARTESIAN_POINT('Ctrl Pts',(-5.60010460206764,-14.3903525501596,
-6.349999999985));
#17694=CARTESIAN_POINT('',(-5.60010460205265,0.,-6.34999999999999));
#17695=CARTESIAN_POINT('',(-6.35,0.,-5.60010460205265));
#17696=CARTESIAN_POINT('',(-5.60010460205265,-15.5,-6.34999999999999));
#17697=CARTESIAN_POINT('Origin',(-5.60010460205265,-15.5,-6.34999999999999));
#17698=CARTESIAN_POINT('',(-2.74757696753127E-15,-15.3773491427837,-6.35));
#17699=CARTESIAN_POINT('Ctrl Pts',(-5.60010460198478,-14.3903525501799,
-6.35));
#17700=CARTESIAN_POINT('Ctrl Pts',(-2.40005222287474,-15.3773491427837,
-6.35));
#17701=CARTESIAN_POINT('Ctrl Pts',(-4.71750321760398E-15,-15.3773491427837,
-6.35));
#17702=CARTESIAN_POINT('',(5.60010460205265,0.,-6.34999999999999));
#17703=CARTESIAN_POINT('',(-5.60010460205265,0.,-6.34999999999999));
#17704=CARTESIAN_POINT('',(5.60010460205265,-14.390352550159,-6.34999999999999));
#17705=CARTESIAN_POINT('',(5.60010460205265,-15.5,-6.34999999999999));
#17706=CARTESIAN_POINT('Ctrl Pts',(-4.71750321760398E-15,-15.3773491427837,
-6.35));
#17707=CARTESIAN_POINT('Ctrl Pts',(2.40005222287474,-15.3773491427837,-6.35));
#17708=CARTESIAN_POINT('Ctrl Pts',(5.6001046019848,-14.3903525501799,-6.35));
#17709=CARTESIAN_POINT('Origin',(6.35,-15.5,-5.60010460205265));
#17710=CARTESIAN_POINT('',(6.35,-14.390352550159,-5.60010460205265));
#17711=CARTESIAN_POINT('Ctrl Pts',(5.60010460206764,-14.3903525501596,-6.34999999998499));
#17712=CARTESIAN_POINT('Ctrl Pts',(5.97505230102632,-14.4058383559469,-5.97505230102632));
#17713=CARTESIAN_POINT('Ctrl Pts',(6.349999999985,-14.3903525501596,-5.60010460206764));
#17714=CARTESIAN_POINT('',(6.35,0.,-5.60010460205265));
#17715=CARTESIAN_POINT('',(6.35,0.,-5.60010460205265));
#17716=CARTESIAN_POINT('',(6.35,-15.5,-5.60010460205265));
#17717=CARTESIAN_POINT('Origin',(6.35,-15.5,5.60010460205265));
#17718=CARTESIAN_POINT('',(6.35,-14.390352550159,5.60010460205265));
#17719=CARTESIAN_POINT('Ctrl Pts',(6.35,-14.3903525501799,-5.60010460198479));
#17720=CARTESIAN_POINT('Ctrl Pts',(6.35,-16.1176005778891,1.55431223447522E-15));
#17721=CARTESIAN_POINT('Ctrl Pts',(6.35,-14.3903525501799,5.60010460198479));
#17722=CARTESIAN_POINT('',(6.35,0.,5.60010460205265));
#17723=CARTESIAN_POINT('',(6.35,0.,5.60010460205265));
#17724=CARTESIAN_POINT('',(6.35,-15.5,5.60010460205265));
#17725=CARTESIAN_POINT('',(6.35,-7.99999999999999,2.8));
#17726=CARTESIAN_POINT('Origin',(6.35,-7.99999999999999,0.));
#17727=CARTESIAN_POINT('Origin',(5.60010460205265,-15.5,6.34999999999999));
#17728=CARTESIAN_POINT('Ctrl Pts',(6.34999999998501,-14.3903525501596,5.60010460206765));
#17729=CARTESIAN_POINT('Ctrl Pts',(5.97505230102634,-14.4058383559469,5.97505230102632));
#17730=CARTESIAN_POINT('Ctrl Pts',(5.60010460206767,-14.3903525501596,6.34999999998498));
#17731=CARTESIAN_POINT('',(5.60010460205265,0.,6.34999999999999));
#17732=CARTESIAN_POINT('Origin',(0.,0.,0.));
#17733=CARTESIAN_POINT('',(0.,2.99999999999999,17.85));
#17734=CARTESIAN_POINT('Origin',(0.,2.99999999999999,0.));
#17735=CARTESIAN_POINT('',(0.,9.79999999999999,17.85));
#17736=CARTESIAN_POINT('',(-2.18599453647803E-15,0.,17.85));
#17737=CARTESIAN_POINT('',(-6.98315068203329E-17,18.1,17.85));
#17738=CARTESIAN_POINT('',(8.24516586553328E-17,0.,17.85));
#17739=CARTESIAN_POINT('',(-2.18599453647803E-15,19.5,17.85));
#17740=CARTESIAN_POINT('',(-2.18599453647803E-15,0.,17.85));
#17741=CARTESIAN_POINT('Origin',(0.,19.5,0.));
#17742=CARTESIAN_POINT('',(-6.98315068203329E-17,18.1,-17.85));
#17743=CARTESIAN_POINT('Origin',(0.,18.1,0.));
#17744=CARTESIAN_POINT('',(0.,9.79999999999999,-17.85));
#17745=CARTESIAN_POINT('',(8.24516586553328E-17,0.,-17.85));
#17746=CARTESIAN_POINT('Origin',(0.,9.79999999999999,0.));
#17747=CARTESIAN_POINT('Origin',(0.,24.,0.));
#17748=CARTESIAN_POINT('',(-2.44929359829471E-15,24.,20.));
#17749=CARTESIAN_POINT('Origin',(0.,24.,0.));
#17750=CARTESIAN_POINT('',(-1.83697019872103E-15,24.,-15.));
#17751=CARTESIAN_POINT('Origin',(0.,24.,0.));
#17752=CARTESIAN_POINT('Origin',(0.,0.,0.));
#17753=CARTESIAN_POINT('',(0.,20.,-20.));
#17754=CARTESIAN_POINT('',(-2.44929359829471E-15,20.,20.));
#17755=CARTESIAN_POINT('Origin',(0.,20.,0.));
#17756=CARTESIAN_POINT('',(-2.44929359829471E-15,0.,20.));
#17757=CARTESIAN_POINT('Origin',(0.,20.,0.));
#17758=CARTESIAN_POINT('Origin',(20.,19.5,0.));
#17759=CARTESIAN_POINT('',(0.,19.5,-19.5));
#17760=CARTESIAN_POINT('Origin',(0.,19.5,0.));
#17761=CARTESIAN_POINT('Origin',(0.,20.8,0.));
#17762=CARTESIAN_POINT('',(-1.83697019872103E-15,20.8,-15.));
#17763=CARTESIAN_POINT('Origin',(0.,20.8,0.));
#17764=CARTESIAN_POINT('',(-1.83697019872103E-15,20.8,-15.));
#17765=CARTESIAN_POINT('Origin',(0.,20.8,0.));
#17766=CARTESIAN_POINT('',(-6.73555739531046E-16,20.8,-5.50000000000002));
#17767=CARTESIAN_POINT('Origin',(0.,20.8,0.));
#17768=CARTESIAN_POINT('',(10.9,20.8,-3.));
#17769=CARTESIAN_POINT('Origin',(10.9,20.8,0.));
#17770=CARTESIAN_POINT('Origin',(0.,1.3,-17.85));
#17771=CARTESIAN_POINT('',(0.,1.3,17.85));
#17772=CARTESIAN_POINT('Origin',(0.,1.3,0.));
#17773=CARTESIAN_POINT('',(-2.02066721859313E-15,1.29999999999999,-16.5));
#17774=CARTESIAN_POINT('Origin',(0.,1.3,0.));
#17775=CARTESIAN_POINT('Origin',(0.,19.5,0.));
#17776=CARTESIAN_POINT('',(-2.02066721859313E-15,2.99999999999999,-16.5));
#17777=CARTESIAN_POINT('Origin',(0.,2.99999999999999,0.));
#17778=CARTESIAN_POINT('',(-2.02066721859313E-15,19.5,-16.5));
#17779=CARTESIAN_POINT('Origin',(0.,3.,-17.85));
#17780=CARTESIAN_POINT('Origin',(17.85,0.,0.));
#17781=CARTESIAN_POINT('',(-2.18599453647803E-15,0.,17.85));
#17782=CARTESIAN_POINT('Origin',(0.,0.,0.));
#17783=CARTESIAN_POINT('Origin',(0.,0.,0.));
#17784=CARTESIAN_POINT('',(-2.18599453647803E-15,0.,17.85));
#17785=CARTESIAN_POINT('Origin',(10.9,6.89999999999999,0.));
#17786=CARTESIAN_POINT('',(10.9,18.1,-3.));
#17787=CARTESIAN_POINT('Origin',(10.9,18.1,0.));
#17788=CARTESIAN_POINT('',(10.9,6.89999999999999,-3.));
#17789=CARTESIAN_POINT('Origin',(0.,6.89999999999999,0.));
#17790=CARTESIAN_POINT('',(-6.12323399573677E-16,6.89999999999999,-5.));
#17791=CARTESIAN_POINT('Origin',(0.,6.89999999999999,0.));
#17792=CARTESIAN_POINT('',(0.,9.79999999999999,-5.));
#17793=CARTESIAN_POINT('',(-6.12323399573677E-16,6.89999999999999,-5.));
#17794=CARTESIAN_POINT('',(-6.98315068203329E-17,18.1,-5.));
#17795=CARTESIAN_POINT('',(2.43989602143332E-17,6.89999999999999,-5.));
#17796=CARTESIAN_POINT('',(-6.12323399573677E-16,20.3,-5.));
#17797=CARTESIAN_POINT('',(-6.12323399573677E-16,6.89999999999999,-5.));
#17798=CARTESIAN_POINT('Origin',(0.,20.3,0.));
#17799=CARTESIAN_POINT('',(-6.98315068203329E-17,18.1,5.));
#17800=CARTESIAN_POINT('Origin',(0.,18.1,0.));
#17801=CARTESIAN_POINT('',(0.,9.79999999999999,5.));
#17802=CARTESIAN_POINT('',(2.43989602143332E-17,6.89999999999999,5.));
#17803=CARTESIAN_POINT('Origin',(0.,9.79999999999999,0.));
#17804=CARTESIAN_POINT('Origin',(0.,6.89999999999999,0.));
#17805=CARTESIAN_POINT('Origin',(17.85,9.8,-20.));
#17806=CARTESIAN_POINT('',(0.,9.79999999999999,-20.));
#17807=CARTESIAN_POINT('',(0.,9.79999999999999,-20.));
#17808=CARTESIAN_POINT('',(10.9,9.79999999999999,-3.));
#17809=CARTESIAN_POINT('Origin',(10.9,9.79999999999999,0.));
#17810=CARTESIAN_POINT('Origin',(-6.98315068203329E-17,18.1,-20.));
#17811=CARTESIAN_POINT('',(-6.98315068203329E-17,18.1,-20.));
#17812=CARTESIAN_POINT('Origin',(-6.98315068203329E-17,18.1,-20.));
#17813=CARTESIAN_POINT('',(-6.98315068203329E-17,18.1,-20.));
#17814=CARTESIAN_POINT('Origin',(17.85,18.1,-20.));
#17815=CARTESIAN_POINT('Origin',(10.9,6.89999999999999,0.));
#17816=CARTESIAN_POINT('',(10.9,6.89999999999999,-3.));
#17817=CARTESIAN_POINT('Origin',(10.9,6.89999999999999,0.));
#17818=CARTESIAN_POINT('Origin',(10.9,6.89999999999999,0.));
#17819=CARTESIAN_POINT('',(10.9,6.89999999999999,-3.));
#17820=CARTESIAN_POINT('Origin',(-3.65,-7.99999999999999,0.));
#17821=CARTESIAN_POINT('',(-3.65,-7.99999999999999,2.8));
#17822=CARTESIAN_POINT('Origin',(-3.65,-7.99999999999999,0.));
#17823=CARTESIAN_POINT('',(-3.65,-7.99999999999999,2.8));
#17824=CARTESIAN_POINT('Origin',(-3.65,-7.99999999999999,0.));
#17825=CARTESIAN_POINT('Origin',(0.,-15.5,0.));
#17826=CARTESIAN_POINT('',(0.,-15.5,-6.08697438789325));
#17827=CARTESIAN_POINT('',(-7.45439370062539E-16,-15.5,-6.08697438789325));
#17828=CARTESIAN_POINT('Origin',(0.,-15.5,0.));
#17829=CARTESIAN_POINT('Origin',(0.,-15.5,0.));
#17830=CARTESIAN_POINT('Origin',(0.,19.5,0.));
#17831=CARTESIAN_POINT('',(-2.38806125833734E-15,19.5,-19.5));
#17832=CARTESIAN_POINT('Origin',(0.,20.3,0.));
#17833=CARTESIAN_POINT('',(-6.12323399573677E-16,20.3,-5.));
#32956=UNCERTAINTY_MEASURE_WITH_UNIT(LENGTH_MEASURE(0.01),#33017,
'DISTANCE_ACCURACY_VALUE',
'Maximum model space distance between geometric entities at asserted c
onnectivities');
#32984=UNCERTAINTY_MEASURE_WITH_UNIT(LENGTH_MEASURE(0.01),#33017,
'DISTANCE_ACCURACY_VALUE',
'Maximum model space distance between geometric entities at asserted c
onnectivities');
#32988=(
GEOMETRIC_REPRESENTATION_CONTEXT(3)
GLOBAL_UNCERTAINTY_ASSIGNED_CONTEXT((#32956))
GLOBAL_UNIT_ASSIGNED_CONTEXT((#33017,#33019,#33020))
REPRESENTATION_CONTEXT('','3D')
);
#33016=(
GEOMETRIC_REPRESENTATION_CONTEXT(3)
GLOBAL_UNCERTAINTY_ASSIGNED_CONTEXT((#32984))
GLOBAL_UNIT_ASSIGNED_CONTEXT((#33017,#33019,#33020))
REPRESENTATION_CONTEXT('','3D')
);
#33017=(
LENGTH_UNIT()
NAMED_UNIT(*)
SI_UNIT(.MILLI.,.METRE.)
);
#33019=(
NAMED_UNIT(*)
PLANE_ANGLE_UNIT()
SI_UNIT($,.RADIAN.)
);
#33020=(
NAMED_UNIT(*)
SI_UNIT($,.STERADIAN.)
SOLID_ANGLE_UNIT()
);
#33024=SHAPE_DEFINITION_REPRESENTATION(#33055,#33127);
#33055=PRODUCT_DEFINITION_SHAPE('',$,#33159);
#33127=SHAPE_REPRESENTATION('',(#10519),#32988);
#33155=PRODUCT_DEFINITION_CONTEXT('part definition',#33250,'design');
#33159=PRODUCT_DEFINITION(
'P_Torque Wrench_Housing_PRT-RH-1004-02_M_Rev01','PRT-RH-1004-02',#33190,
#33155);
#33190=PRODUCT_DEFINITION_FORMATION('',$,#33255);
#33250=APPLICATION_CONTEXT(
'Core Data for Automotive Mechanical Design Process');
#33251=PRODUCT_CONTEXT('part definition',#33250,'mechanical');
#33255=PRODUCT('P_Torque Wrench_Housing_PRT-RH-1004-02_M_Rev01',
'PRT-RH-1004-02',$,(#33251));
#33284=PRESENTATION_STYLE_ASSIGNMENT((#33291));
#33291=SURFACE_STYLE_USAGE(.BOTH.,#33298);
#33298=SURFACE_SIDE_STYLE('',(#33305));
#33305=SURFACE_STYLE_FILL_AREA(#33312);
#33312=FILL_AREA_STYLE('Opaque(186,91,6)',(#33319));
#33319=FILL_AREA_STYLE_COLOUR('Opaque(186,91,6)',#33326);
#33326=COLOUR_RGB('Opaque(186,91,6)', 0.09019608, 0.27058824, 0.51372549);
ENDSEC;
END-ISO-10303-21;
